ISO-10303-21;
HEADER;
/* Generated by software containing ST-Developer
 * from STEP Tools, Inc. (www.steptools.com) 
 */

FILE_DESCRIPTION(
/* description */ ('Torque wrench calibration arm'),
/* implementation_level */ '2;1');

FILE_NAME(
/* name */ 'Hanger outer shim (1).step',
/* time_stamp */ '2026-10-28T03:24:52-07:00',
/* author */ (''),
/* organization */ (''),
/* preprocessor_version */ 'ST-DEVELOPER v20.2',
/* originating_system */ 'Autodesk Translation Framework v15.17.0.0',
/* authorisation */ '');

FILE_SCHEMA (('AUTOMOTIVE_DESIGN { 1 0 10303 214 3 1 1 }'));
ENDSEC;

DATA;
#10=MECHANICAL_DESIGN_GEOMETRIC_PRESENTATION_REPRESENTATION('',(#476),#12783);
#385=SHAPE_REPRESENTATION_RELATIONSHIP('SRR','None',#12970,#422);
#422=ADVANCED_BREP_SHAPE_REPRESENTATION('',(#528),#12779);
#476=STYLED_ITEM('',(#13205),#528);
#528=MANIFOLD_SOLID_BREP('Body1',#6547);
#645=FACE_BOUND('',#1754,.T.);
#646=FACE_BOUND('',#1756,.T.);
#858=PLANE('',#7753);
#859=PLANE('',#7754);
#1242=FACE_OUTER_BOUND('',#1751,.T.);
#1243=FACE_OUTER_BOUND('',#1752,.T.);
#1244=FACE_OUTER_BOUND('',#1753,.T.);
#1245=FACE_OUTER_BOUND('',#1755,.T.);
#1751=EDGE_LOOP('',(#5891,#5892,#5893,#5894));
#1752=EDGE_LOOP('',(#5895,#5896,#5897,#5898));
#1753=EDGE_LOOP('',(#5899));
#1754=EDGE_LOOP('',(#5900));
#1755=EDGE_LOOP('',(#5901));
#1756=EDGE_LOOP('',(#5902));
#2172=LINE('',#12577,#2587);
#2173=LINE('',#12583,#2588);
#2587=VECTOR('',#9774,0.505000000000003);
#2588=VECTOR('',#9781,0.700000000000003);
#2952=CIRCLE('',#7748,0.505000000000003);
#2953=CIRCLE('',#7749,0.505000000000003);
#2954=CIRCLE('',#7751,0.700000000000003);
#2955=CIRCLE('',#7752,0.700000000000003);
#3502=VERTEX_POINT('',#12574);
#3503=VERTEX_POINT('',#12576);
#3504=VERTEX_POINT('',#12580);
#3505=VERTEX_POINT('',#12582);
#4303=EDGE_CURVE('',#3502,#3502,#2952,.T.);
#4304=EDGE_CURVE('',#3502,#3503,#2172,.T.);
#4305=EDGE_CURVE('',#3503,#3503,#2953,.T.);
#4306=EDGE_CURVE('',#3504,#3504,#2954,.T.);
#4307=EDGE_CURVE('',#3504,#3505,#2173,.T.);
#4308=EDGE_CURVE('',#3505,#3505,#2955,.T.);
#5891=ORIENTED_EDGE('',*,*,#4303,.F.);
#5892=ORIENTED_EDGE('',*,*,#4304,.T.);
#5893=ORIENTED_EDGE('',*,*,#4305,.T.);
#5894=ORIENTED_EDGE('',*,*,#4304,.F.);
#5895=ORIENTED_EDGE('',*,*,#4306,.F.);
#5896=ORIENTED_EDGE('',*,*,#4307,.T.);
#5897=ORIENTED_EDGE('',*,*,#4308,.T.);
#5898=ORIENTED_EDGE('',*,*,#4307,.F.);
#5899=ORIENTED_EDGE('',*,*,#4306,.T.);
#5900=ORIENTED_EDGE('',*,*,#4303,.T.);
#5901=ORIENTED_EDGE('',*,*,#4308,.F.);
#5902=ORIENTED_EDGE('',*,*,#4305,.F.);
#6092=CYLINDRICAL_SURFACE('',#7747,0.505000000000003);
#6093=CYLINDRICAL_SURFACE('',#7750,0.700000000000003);
#6467=ADVANCED_FACE('',(#1242),#6092,.F.);
#6468=ADVANCED_FACE('',(#1243),#6093,.T.);
#6469=ADVANCED_FACE('',(#1244,#645),#858,.T.);
#6470=ADVANCED_FACE('',(#1245,#646),#859,.F.);
#6547=CLOSED_SHELL('',(#6467,#6468,#6469,#6470));
#7746=AXIS2_PLACEMENT_3D('',#12572,#9768,#9769);
#7747=AXIS2_PLACEMENT_3D('',#12573,#9770,#9771);
#7748=AXIS2_PLACEMENT_3D('',#12575,#9772,#9773);
#7749=AXIS2_PLACEMENT_3D('',#12578,#9775,#9776);
#7750=AXIS2_PLACEMENT_3D('',#12579,#9777,#9778);
#7751=AXIS2_PLACEMENT_3D('',#12581,#9779,#9780);
#7752=AXIS2_PLACEMENT_3D('',#12584,#9782,#9783);
#7753=AXIS2_PLACEMENT_3D('',#12585,#9784,#9785);
#7754=AXIS2_PLACEMENT_3D('',#12586,#9786,#9787);
#9768=DIRECTION('axis',(0.,0.,1.));
#9769=DIRECTION('refdir',(1.,0.,0.));
#9770=DIRECTION('center_axis',(0.,1.,0.));
#9771=DIRECTION('ref_axis',(1.,0.,0.));
#9772=DIRECTION('center_axis',(0.,-1.,0.));
#9773=DIRECTION('ref_axis',(1.,0.,0.));
#9774=DIRECTION('',(0.,-1.,0.));
#9775=DIRECTION('center_axis',(0.,-1.,0.));
#9776=DIRECTION('ref_axis',(1.,0.,0.));
#9777=DIRECTION('center_axis',(0.,1.,0.));
#9778=DIRECTION('ref_axis',(1.,0.,0.));
#9779=DIRECTION('center_axis',(0.,1.,0.));
#9780=DIRECTION('ref_axis',(1.,0.,0.));
#9781=DIRECTION('',(0.,-1.,0.));
#9782=DIRECTION('center_axis',(0.,1.,0.));
#9783=DIRECTION('ref_axis',(1.,0.,0.));
#9784=DIRECTION('center_axis',(0.,1.,0.));
#9785=DIRECTION('ref_axis',(1.,0.,0.));
#9786=DIRECTION('center_axis',(0.,1.,0.));
#9787=DIRECTION('ref_axis',(1.,0.,0.));
#12572=CARTESIAN_POINT('',(0.,0.,0.));
#12573=CARTESIAN_POINT('Origin',(50.,10.2,8.));
#12574=CARTESIAN_POINT('',(49.495,10.4,8.));
#12575=CARTESIAN_POINT('Origin',(50.,10.4,8.));
#12576=CARTESIAN_POINT('',(49.495,10.2,8.));
#12577=CARTESIAN_POINT('',(49.495,10.2,8.));
#12578=CARTESIAN_POINT('Origin',(50.,10.2,8.));
#12579=CARTESIAN_POINT('Origin',(50.,10.2,8.));
#12580=CARTESIAN_POINT('',(49.3,10.4,8.));
#12581=CARTESIAN_POINT('Origin',(50.,10.4,8.));
#12582=CARTESIAN_POINT('',(49.3,10.2,8.));
#12583=CARTESIAN_POINT('',(49.3,10.2,8.));
#12584=CARTESIAN_POINT('Origin',(50.,10.2,8.));
#12585=CARTESIAN_POINT('Origin',(50.,10.4,8.));
#12586=CARTESIAN_POINT('Origin',(50.,10.2,8.));
#12735=UNCERTAINTY_MEASURE_WITH_UNIT(LENGTH_MEASURE(0.001),#12784,
'DISTANCE_ACCURACY_VALUE',
'Maximum model space distance between geometric entities at asserted c
onnectivities');
#12739=UNCERTAINTY_MEASURE_WITH_UNIT(LENGTH_MEASURE(0.001),#12784,
'DISTANCE_ACCURACY_VALUE',
'Maximum model space distance between geometric entities at asserted c
onnectivities');
#12779=(
GEOMETRIC_REPRESENTATION_CONTEXT(3)
GLOBAL_UNCERTAINTY_ASSIGNED_CONTEXT((#12735))
GLOBAL_UNIT_ASSIGNED_CONTEXT((#12784,#12786,#12787))
REPRESENTATION_CONTEXT('','3D')
);
#12783=(
GEOMETRIC_REPRESENTATION_CONTEXT(3)
GLOBAL_UNCERTAINTY_ASSIGNED_CONTEXT((#12739))
GLOBAL_UNIT_ASSIGNED_CONTEXT((#12784,#12786,#12787))
REPRESENTATION_CONTEXT('','3D')
);
#12784=(
LENGTH_UNIT()
NAMED_UNIT(*)
SI_UNIT(.CENTI.,.METRE.)
);
#12786=(
NAMED_UNIT(*)
PLANE_ANGLE_UNIT()
SI_UNIT($,.RADIAN.)
);
#12787=(
NAMED_UNIT(*)
SI_UNIT($,.STERADIAN.)
SOLID_ANGLE_UNIT()
);
#12827=SHAPE_DEFINITION_REPRESENTATION(#12914,#12970);
#12914=PRODUCT_DEFINITION_SHAPE('',$,#13014);
#12970=SHAPE_REPRESENTATION('',(#7746),#12779);
#12974=PRODUCT_DEFINITION_CONTEXT('part definition',#13105,'design');
#13014=PRODUCT_DEFINITION('Hanger outer shim (1)','Hanger outer shim (1)',
#13057,#12974);
#13057=PRODUCT_DEFINITION_FORMATION('',$,#13146);
#13105=APPLICATION_CONTEXT(
'Core Data for Automotive Mechanical Design Process');
#13106=PRODUCT_CONTEXT('part definition',#13105,'mechanical');
#13146=PRODUCT('Hanger outer shim (1)','Hanger outer shim (1)',
'Hanger outer shim (1)',(#13106));
#13199=COLOUR_RGB('Sky Blue',0.24,0.69,0.87);
#13200=FILL_AREA_STYLE_COLOUR('',#13199);
#13201=FILL_AREA_STYLE('',(#13200));
#13202=SURFACE_STYLE_FILL_AREA(#13201);
#13203=SURFACE_SIDE_STYLE('',(#13202));
#13204=SURFACE_STYLE_USAGE(.BOTH.,#13203);
#13205=PRESENTATION_STYLE_ASSIGNMENT((#13204));
ENDSEC;
END-ISO-10303-21;
